ISO-10303-21;
HEADER;
/* Generated by software containing ST-Developer
 * from STEP Tools, Inc. (www.steptools.com) 
 */

FILE_DESCRIPTION(
/* description */ ('PAT-091'),
/* implementation_level */ '2;1');

FILE_NAME(
/* name */ 'Axle end keeper (8).step',
/* time_stamp */ '2026-10-27T15:34:44-07:00',
/* author */ (''),
/* organization */ (''),
/* preprocessor_version */ 'ST-DEVELOPER v20.2',
/* originating_system */ 'Autodesk Translation Framework v15.17.0.0',
/* authorisation */ '');

FILE_SCHEMA (('AUTOMOTIVE_DESIGN { 1 0 10303 214 3 1 1 }'));
ENDSEC;

DATA;
#10=MECHANICAL_DESIGN_GEOMETRIC_PRESENTATION_REPRESENTATION('',(#1036),#25100);
#816=SHAPE_REPRESENTATION_RELATIONSHIP('SRR','None',#25582,#926);
#926=ADVANCED_BREP_SHAPE_REPRESENTATION('',(#1158),#25052);
#1036=STYLED_ITEM('',(#26191),#1158);
#1158=MANIFOLD_SOLID_BREP('Body1',#13315);
#1510=FACE_BOUND('',#3684,.T.);
#1511=FACE_BOUND('',#3686,.T.);
#1923=PLANE('',#15617);
#1924=PLANE('',#15618);
#2568=FACE_OUTER_BOUND('',#3681,.T.);
#2569=FACE_OUTER_BOUND('',#3682,.T.);
#2570=FACE_OUTER_BOUND('',#3683,.T.);
#2571=FACE_OUTER_BOUND('',#3685,.T.);
#3681=EDGE_LOOP('',(#10996,#10997,#10998,#10999));
#3682=EDGE_LOOP('',(#11000,#11001,#11002,#11003));
#3683=EDGE_LOOP('',(#11004));
#3684=EDGE_LOOP('',(#11005));
#3685=EDGE_LOOP('',(#11006));
#3686=EDGE_LOOP('',(#11007));
#4686=LINE('',#23294,#5426);
#4687=LINE('',#23300,#5427);
#5426=VECTOR('',#19086,0.225000000000001);
#5427=VECTOR('',#19093,1.);
#6050=CIRCLE('',#15612,0.225000000000001);
#6051=CIRCLE('',#15613,0.225000000000001);
#6052=CIRCLE('',#15615,1.);
#6053=CIRCLE('',#15616,1.);
#7055=VERTEX_POINT('',#23291);
#7056=VERTEX_POINT('',#23293);
#7057=VERTEX_POINT('',#23297);
#7058=VERTEX_POINT('',#23299);
#8433=EDGE_CURVE('',#7055,#7055,#6050,.T.);
#8434=EDGE_CURVE('',#7055,#7056,#4686,.T.);
#8435=EDGE_CURVE('',#7056,#7056,#6051,.T.);
#8436=EDGE_CURVE('',#7057,#7057,#6052,.T.);
#8437=EDGE_CURVE('',#7057,#7058,#4687,.T.);
#8438=EDGE_CURVE('',#7058,#7058,#6053,.T.);
#10996=ORIENTED_EDGE('',*,*,#8433,.F.);
#10997=ORIENTED_EDGE('',*,*,#8434,.T.);
#10998=ORIENTED_EDGE('',*,*,#8435,.T.);
#10999=ORIENTED_EDGE('',*,*,#8434,.F.);
#11000=ORIENTED_EDGE('',*,*,#8436,.F.);
#11001=ORIENTED_EDGE('',*,*,#8437,.T.);
#11002=ORIENTED_EDGE('',*,*,#8438,.T.);
#11003=ORIENTED_EDGE('',*,*,#8437,.F.);
#11004=ORIENTED_EDGE('',*,*,#8436,.T.);
#11005=ORIENTED_EDGE('',*,*,#8433,.T.);
#11006=ORIENTED_EDGE('',*,*,#8438,.F.);
#11007=ORIENTED_EDGE('',*,*,#8435,.F.);
#12288=CYLINDRICAL_SURFACE('',#15611,0.225000000000001);
#12289=CYLINDRICAL_SURFACE('',#15614,1.);
#12935=ADVANCED_FACE('',(#2568),#12288,.F.);
#12936=ADVANCED_FACE('',(#2569),#12289,.T.);
#12937=ADVANCED_FACE('',(#2570,#1510),#1923,.T.);
#12938=ADVANCED_FACE('',(#2571,#1511),#1924,.F.);
#13315=CLOSED_SHELL('',(#12935,#12936,#12937,#12938));
#15610=AXIS2_PLACEMENT_3D('',#23289,#19080,#19081);
#15611=AXIS2_PLACEMENT_3D('',#23290,#19082,#19083);
#15612=AXIS2_PLACEMENT_3D('',#23292,#19084,#19085);
#15613=AXIS2_PLACEMENT_3D('',#23295,#19087,#19088);
#15614=AXIS2_PLACEMENT_3D('',#23296,#19089,#19090);
#15615=AXIS2_PLACEMENT_3D('',#23298,#19091,#19092);
#15616=AXIS2_PLACEMENT_3D('',#23301,#19094,#19095);
#15617=AXIS2_PLACEMENT_3D('',#23302,#19096,#19097);
#15618=AXIS2_PLACEMENT_3D('',#23303,#19098,#19099);
#19080=DIRECTION('axis',(0.,0.,1.));
#19081=DIRECTION('refdir',(1.,0.,0.));
#19082=DIRECTION('center_axis',(0.,1.,0.));
#19083=DIRECTION('ref_axis',(1.,0.,0.));
#19084=DIRECTION('center_axis',(0.,-1.,0.));
#19085=DIRECTION('ref_axis',(1.,0.,0.));
#19086=DIRECTION('',(0.,-1.,0.));
#19087=DIRECTION('center_axis',(0.,-1.,0.));
#19088=DIRECTION('ref_axis',(1.,0.,0.));
#19089=DIRECTION('center_axis',(0.,1.,0.));
#19090=DIRECTION('ref_axis',(1.,0.,0.));
#19091=DIRECTION('center_axis',(0.,1.,0.));
#19092=DIRECTION('ref_axis',(1.,0.,0.));
#19093=DIRECTION('',(0.,-1.,0.));
#19094=DIRECTION('center_axis',(0.,1.,0.));
#19095=DIRECTION('ref_axis',(1.,0.,0.));
#19096=DIRECTION('center_axis',(0.,1.,0.));
#19097=DIRECTION('ref_axis',(1.,0.,0.));
#19098=DIRECTION('center_axis',(0.,1.,0.));
#19099=DIRECTION('ref_axis',(1.,0.,0.));
#23289=CARTESIAN_POINT('',(0.,0.,0.));
#23290=CARTESIAN_POINT('Origin',(19.3649167310371,-7.7,8.));
#23291=CARTESIAN_POINT('',(19.1399167310371,-7.5,8.));
#23292=CARTESIAN_POINT('Origin',(19.3649167310371,-7.5,8.));
#23293=CARTESIAN_POINT('',(19.1399167310371,-7.7,8.));
#23294=CARTESIAN_POINT('',(19.1399167310371,-7.7,8.));
#23295=CARTESIAN_POINT('Origin',(19.3649167310371,-7.7,8.));
#23296=CARTESIAN_POINT('Origin',(19.3649167310371,-7.7,8.));
#23297=CARTESIAN_POINT('',(18.3649167310371,-7.5,8.));
#23298=CARTESIAN_POINT('Origin',(19.3649167310371,-7.5,8.));
#23299=CARTESIAN_POINT('',(18.3649167310371,-7.7,8.));
#23300=CARTESIAN_POINT('',(18.3649167310371,-7.7,8.));
#23301=CARTESIAN_POINT('Origin',(19.3649167310371,-7.7,8.));
#23302=CARTESIAN_POINT('Origin',(19.3649167310371,-7.5,8.));
#23303=CARTESIAN_POINT('Origin',(19.3649167310371,-7.7,8.));
#24931=UNCERTAINTY_MEASURE_WITH_UNIT(LENGTH_MEASURE(0.001),#25101,
'DISTANCE_ACCURACY_VALUE',
'Maximum model space distance between geometric entities at asserted c
onnectivities');
#24979=UNCERTAINTY_MEASURE_WITH_UNIT(LENGTH_MEASURE(0.001),#25101,
'DISTANCE_ACCURACY_VALUE',
'Maximum model space distance between geometric entities at asserted c
onnectivities');
#25052=(
GEOMETRIC_REPRESENTATION_CONTEXT(3)
GLOBAL_UNCERTAINTY_ASSIGNED_CONTEXT((#24931))
GLOBAL_UNIT_ASSIGNED_CONTEXT((#25101,#25103,#25104))
REPRESENTATION_CONTEXT('','3D')
);
#25100=(
GEOMETRIC_REPRESENTATION_CONTEXT(3)
GLOBAL_UNCERTAINTY_ASSIGNED_CONTEXT((#24979))
GLOBAL_UNIT_ASSIGNED_CONTEXT((#25101,#25103,#25104))
REPRESENTATION_CONTEXT('','3D')
);
#25101=(
LENGTH_UNIT()
NAMED_UNIT(*)
SI_UNIT(.CENTI.,.METRE.)
);
#25103=(
NAMED_UNIT(*)
PLANE_ANGLE_UNIT()
SI_UNIT($,.RADIAN.)
);
#25104=(
NAMED_UNIT(*)
SI_UNIT($,.STERADIAN.)
SOLID_ANGLE_UNIT()
);
#25177=SHAPE_DEFINITION_REPRESENTATION(#25299,#25582);
#25299=PRODUCT_DEFINITION_SHAPE('',$,#25703);
#25582=SHAPE_REPRESENTATION('',(#15610),#25052);
#25630=PRODUCT_DEFINITION_CONTEXT('part definition',#25992,'design');
#25703=PRODUCT_DEFINITION('Axle end keeper (8)','Axle end keeper (8)',#25823,
#25630);
#25823=PRODUCT_DEFINITION_FORMATION('',$,#26066);
#25992=APPLICATION_CONTEXT(
'Core Data for Automotive Mechanical Design Process');
#25993=PRODUCT_CONTEXT('part definition',#25992,'mechanical');
#26066=PRODUCT('Axle end keeper (8)','Axle end keeper (8)',
'Axle end keeper (8)',(#25993));
#26185=COLOUR_RGB('Grey',0.48,0.52,0.57);
#26186=FILL_AREA_STYLE_COLOUR('',#26185);
#26187=FILL_AREA_STYLE('',(#26186));
#26188=SURFACE_STYLE_FILL_AREA(#26187);
#26189=SURFACE_SIDE_STYLE('',(#26188));
#26190=SURFACE_STYLE_USAGE(.BOTH.,#26189);
#26191=PRESENTATION_STYLE_ASSIGNMENT((#26190));
ENDSEC;
END-ISO-10303-21;
